ISO-10303-21;
HEADER;
/* Generated by software containing ST-Developer
 * from STEP Tools, Inc. (www.steptools.com) 
 */

FILE_DESCRIPTION(
/* description */ ('STEP AP214'),
/* implementation_level */ '2;1');

FILE_NAME(
/* name */ 'Button Head Cap Screw M3x0.5x3.step',
/* time_stamp */ '2026-11-14T22:03:06-08:00',
/* author */ (''),
/* organization */ (''),
/* preprocessor_version */ 'ST-DEVELOPER v20.2',
/* originating_system */ 'Autodesk Translation Framework v15.17.0.0',
/* authorisation */ '');

FILE_SCHEMA (('AUTOMOTIVE_DESIGN { 1 0 10303 214 3 1 1 }'));
ENDSEC;

DATA;
#10=MECHANICAL_DESIGN_GEOMETRIC_PRESENTATION_REPRESENTATION('',(#314),#12966);
#154=SPHERICAL_SURFACE('',#6170,3.35141684393879);
#158=TOROIDAL_SURFACE('',#6159,1.6,0.1);
#165=CONICAL_SURFACE('',#6152,1732.05080756886,1.04719755119659);
#166=CONICAL_SURFACE('',#6163,1.2195,0.785398163397446);
#294=SHAPE_REPRESENTATION_RELATIONSHIP('SRR','None',#13032,#302);
#302=ADVANCED_BREP_SHAPE_REPRESENTATION('',(#326),#12965);
#314=STYLED_ITEM('',(#13075),#326);
#326=MANIFOLD_SOLID_BREP('Body1',#5589);
#386=FACE_BOUND('',#1216,.T.);
#387=FACE_BOUND('',#1218,.T.);
#388=FACE_BOUND('',#1220,.T.);
#535=PLANE('',#6172);
#536=PLANE('',#6173);
#537=PLANE('',#6174);
#538=PLANE('',#6175);
#539=PLANE('',#6176);
#540=PLANE('',#6177);
#541=PLANE('',#6178);
#542=PLANE('',#6179);
#543=PLANE('',#6180);
#544=PLANE('',#6181);
#545=PLANE('',#6182);
#546=PLANE('',#6183);
#547=PLANE('',#6184);
#548=PLANE('',#6185);
#549=PLANE('',#6186);
#840=FACE_OUTER_BOUND('',#1210,.T.);
#841=FACE_OUTER_BOUND('',#1211,.T.);
#842=FACE_OUTER_BOUND('',#1212,.T.);
#843=FACE_OUTER_BOUND('',#1213,.T.);
#844=FACE_OUTER_BOUND('',#1214,.T.);
#845=FACE_OUTER_BOUND('',#1215,.T.);
#846=FACE_OUTER_BOUND('',#1217,.T.);
#847=FACE_OUTER_BOUND('',#1219,.T.);
#848=FACE_OUTER_BOUND('',#1221,.T.);
#849=FACE_OUTER_BOUND('',#1222,.T.);
#850=FACE_OUTER_BOUND('',#1223,.T.);
#851=FACE_OUTER_BOUND('',#1224,.T.);
#852=FACE_OUTER_BOUND('',#1225,.T.);
#853=FACE_OUTER_BOUND('',#1226,.T.);
#854=FACE_OUTER_BOUND('',#1227,.T.);
#855=FACE_OUTER_BOUND('',#1228,.T.);
#856=FACE_OUTER_BOUND('',#1229,.T.);
#857=FACE_OUTER_BOUND('',#1230,.T.);
#858=FACE_OUTER_BOUND('',#1231,.T.);
#859=FACE_OUTER_BOUND('',#1232,.T.);
#860=FACE_OUTER_BOUND('',#1233,.T.);
#1210=EDGE_LOOP('',(#5089,#5090,#5091,#5092,#5093,#5094,#5095,#5096));
#1211=EDGE_LOOP('',(#5097,#5098,#5099,#5100));
#1212=EDGE_LOOP('',(#5101,#5102,#5103,#5104));
#1213=EDGE_LOOP('',(#5105,#5106,#5107,#5108));
#1214=EDGE_LOOP('',(#5109,#5110,#5111,#5112));
#1215=EDGE_LOOP('',(#5113));
#1216=EDGE_LOOP('',(#5114));
#1217=EDGE_LOOP('',(#5115));
#1218=EDGE_LOOP('',(#5116,#5117,#5118,#5119,#5120,#5121));
#1219=EDGE_LOOP('',(#5122));
#1220=EDGE_LOOP('',(#5123));
#1221=EDGE_LOOP('',(#5124));
#1222=EDGE_LOOP('',(#5125,#5126,#5127,#5128,#5129));
#1223=EDGE_LOOP('',(#5130,#5131,#5132,#5133,#5134));
#1224=EDGE_LOOP('',(#5135,#5136,#5137,#5138,#5139));
#1225=EDGE_LOOP('',(#5140,#5141,#5142,#5143,#5144));
#1226=EDGE_LOOP('',(#5145,#5146,#5147,#5148,#5149));
#1227=EDGE_LOOP('',(#5150,#5151,#5152,#5153,#5154));
#1228=EDGE_LOOP('',(#5155,#5156,#5157));
#1229=EDGE_LOOP('',(#5158,#5159,#5160));
#1230=EDGE_LOOP('',(#5161,#5162,#5163));
#1231=EDGE_LOOP('',(#5164,#5165,#5166));
#1232=EDGE_LOOP('',(#5167,#5168,#5169));
#1233=EDGE_LOOP('',(#5170,#5171,#5172));
#1663=LINE('',#12826,#2120);
#1664=LINE('',#12848,#2121);
#1665=LINE('',#12851,#2122);
#1666=LINE('',#12856,#2123);
#1667=LINE('',#12864,#2124);
#1668=LINE('',#12866,#2125);
#1669=LINE('',#12868,#2126);
#1670=LINE('',#12870,#2127);
#1671=LINE('',#12872,#2128);
#1672=LINE('',#12873,#2129);
#1673=LINE('',#12878,#2130);
#1674=LINE('',#12880,#2131);
#1675=LINE('',#12881,#2132);
#1676=LINE('',#12882,#2133);
#1677=LINE('',#12884,#2134);
#1678=LINE('',#12886,#2135);
#1679=LINE('',#12887,#2136);
#1680=LINE('',#12889,#2137);
#1681=LINE('',#12891,#2138);
#1682=LINE('',#12892,#2139);
#1683=LINE('',#12894,#2140);
#1684=LINE('',#12896,#2141);
#1685=LINE('',#12897,#2142);
#1686=LINE('',#12899,#2143);
#1687=LINE('',#12901,#2144);
#1688=LINE('',#12902,#2145);
#1689=LINE('',#12904,#2146);
#1690=LINE('',#12905,#2147);
#2120=VECTOR('',#7599,1732.05080756886);
#2121=VECTOR('',#7624,1.2195);
#2122=VECTOR('',#7629,1.5);
#2123=VECTOR('',#7634,2.85);
#2124=VECTOR('',#7643,1000.);
#2125=VECTOR('',#7644,1000.);
#2126=VECTOR('',#7645,1000.);
#2127=VECTOR('',#7646,1000.);
#2128=VECTOR('',#7647,1000.);
#2129=VECTOR('',#7648,1000.);
#2130=VECTOR('',#7655,1000.);
#2131=VECTOR('',#7656,1000.);
#2132=VECTOR('',#7657,1000.);
#2133=VECTOR('',#7658,1000.);
#2134=VECTOR('',#7661,1000.);
#2135=VECTOR('',#7662,1000.);
#2136=VECTOR('',#7663,1000.);
#2137=VECTOR('',#7666,1000.);
#2138=VECTOR('',#7667,1000.);
#2139=VECTOR('',#7668,1000.);
#2140=VECTOR('',#7671,1000.);
#2141=VECTOR('',#7672,1000.);
#2142=VECTOR('',#7673,1000.);
#2143=VECTOR('',#7676,1000.);
#2144=VECTOR('',#7677,1000.);
#2145=VECTOR('',#7678,1000.);
#2146=VECTOR('',#7681,1000.);
#2147=VECTOR('',#7682,1000.);
#2362=CIRCLE('',#6153,1.);
#2363=CIRCLE('',#6154,1.);
#2364=CIRCLE('',#6155,1.);
#2365=CIRCLE('',#6156,1.);
#2366=CIRCLE('',#6157,1.);
#2367=CIRCLE('',#6158,1.);
#2368=CIRCLE('',#6160,1.6);
#2369=CIRCLE('',#6161,0.1);
#2370=CIRCLE('',#6162,1.5);
#2371=CIRCLE('',#6164,1.5);
#2372=CIRCLE('',#6165,1.2195);
#2373=CIRCLE('',#6168,2.85);
#2374=CIRCLE('',#6169,2.85);
#2375=CIRCLE('',#6171,1.425);
#2852=VERTEX_POINT('',#12824);
#2853=VERTEX_POINT('',#12825);
#2854=VERTEX_POINT('',#12827);
#2855=VERTEX_POINT('',#12829);
#2856=VERTEX_POINT('',#12831);
#2857=VERTEX_POINT('',#12833);
#2858=VERTEX_POINT('',#12835);
#2859=VERTEX_POINT('',#12839);
#2860=VERTEX_POINT('',#12841);
#2861=VERTEX_POINT('',#12845);
#2862=VERTEX_POINT('',#12847);
#2863=VERTEX_POINT('',#12853);
#2864=VERTEX_POINT('',#12855);
#2865=VERTEX_POINT('',#12859);
#2866=VERTEX_POINT('',#12862);
#2867=VERTEX_POINT('',#12863);
#2868=VERTEX_POINT('',#12865);
#2869=VERTEX_POINT('',#12867);
#2870=VERTEX_POINT('',#12869);
#2871=VERTEX_POINT('',#12871);
#2872=VERTEX_POINT('',#12877);
#2873=VERTEX_POINT('',#12879);
#2874=VERTEX_POINT('',#12885);
#2875=VERTEX_POINT('',#12890);
#2876=VERTEX_POINT('',#12895);
#2877=VERTEX_POINT('',#12900);
#3601=EDGE_CURVE('',#2852,#2853,#1663,.T.);
#3602=EDGE_CURVE('',#2853,#2854,#2362,.T.);
#3603=EDGE_CURVE('',#2854,#2855,#2363,.T.);
#3604=EDGE_CURVE('',#2855,#2856,#2364,.T.);
#3605=EDGE_CURVE('',#2856,#2857,#2365,.T.);
#3606=EDGE_CURVE('',#2857,#2858,#2366,.T.);
#3607=EDGE_CURVE('',#2858,#2853,#2367,.T.);
#3608=EDGE_CURVE('',#2859,#2859,#2368,.T.);
#3609=EDGE_CURVE('',#2859,#2860,#2369,.T.);
#3610=EDGE_CURVE('',#2860,#2860,#2370,.T.);
#3611=EDGE_CURVE('',#2861,#2861,#2371,.T.);
#3612=EDGE_CURVE('',#2861,#2862,#1664,.T.);
#3613=EDGE_CURVE('',#2862,#2862,#2372,.T.);
#3614=EDGE_CURVE('',#2860,#2861,#1665,.T.);
#3615=EDGE_CURVE('',#2863,#2863,#2373,.T.);
#3616=EDGE_CURVE('',#2863,#2864,#1666,.T.);
#3617=EDGE_CURVE('',#2864,#2864,#2374,.T.);
#3618=EDGE_CURVE('',#2865,#2865,#2375,.T.);
#3619=EDGE_CURVE('',#2866,#2867,#1667,.T.);
#3620=EDGE_CURVE('',#2867,#2868,#1668,.T.);
#3621=EDGE_CURVE('',#2868,#2869,#1669,.T.);
#3622=EDGE_CURVE('',#2869,#2870,#1670,.T.);
#3623=EDGE_CURVE('',#2870,#2871,#1671,.T.);
#3624=EDGE_CURVE('',#2871,#2866,#1672,.T.);
#3625=EDGE_CURVE('',#2872,#2855,#1673,.T.);
#3626=EDGE_CURVE('',#2855,#2873,#1674,.T.);
#3627=EDGE_CURVE('',#2873,#2868,#1675,.T.);
#3628=EDGE_CURVE('',#2872,#2867,#1676,.T.);
#3629=EDGE_CURVE('',#2873,#2854,#1677,.T.);
#3630=EDGE_CURVE('',#2854,#2874,#1678,.T.);
#3631=EDGE_CURVE('',#2874,#2869,#1679,.T.);
#3632=EDGE_CURVE('',#2874,#2853,#1680,.T.);
#3633=EDGE_CURVE('',#2853,#2875,#1681,.T.);
#3634=EDGE_CURVE('',#2875,#2870,#1682,.T.);
#3635=EDGE_CURVE('',#2875,#2858,#1683,.T.);
#3636=EDGE_CURVE('',#2858,#2876,#1684,.T.);
#3637=EDGE_CURVE('',#2876,#2871,#1685,.T.);
#3638=EDGE_CURVE('',#2876,#2857,#1686,.T.);
#3639=EDGE_CURVE('',#2857,#2877,#1687,.T.);
#3640=EDGE_CURVE('',#2877,#2866,#1688,.T.);
#3641=EDGE_CURVE('',#2877,#2856,#1689,.T.);
#3642=EDGE_CURVE('',#2856,#2872,#1690,.T.);
#5089=ORIENTED_EDGE('',*,*,#3601,.T.);
#5090=ORIENTED_EDGE('',*,*,#3602,.T.);
#5091=ORIENTED_EDGE('',*,*,#3603,.T.);
#5092=ORIENTED_EDGE('',*,*,#3604,.T.);
#5093=ORIENTED_EDGE('',*,*,#3605,.T.);
#5094=ORIENTED_EDGE('',*,*,#3606,.T.);
#5095=ORIENTED_EDGE('',*,*,#3607,.T.);
#5096=ORIENTED_EDGE('',*,*,#3601,.F.);
#5097=ORIENTED_EDGE('',*,*,#3608,.F.);
#5098=ORIENTED_EDGE('',*,*,#3609,.T.);
#5099=ORIENTED_EDGE('',*,*,#3610,.F.);
#5100=ORIENTED_EDGE('',*,*,#3609,.F.);
#5101=ORIENTED_EDGE('',*,*,#3611,.F.);
#5102=ORIENTED_EDGE('',*,*,#3612,.T.);
#5103=ORIENTED_EDGE('',*,*,#3613,.T.);
#5104=ORIENTED_EDGE('',*,*,#3612,.F.);
#5105=ORIENTED_EDGE('',*,*,#3610,.T.);
#5106=ORIENTED_EDGE('',*,*,#3614,.T.);
#5107=ORIENTED_EDGE('',*,*,#3611,.T.);
#5108=ORIENTED_EDGE('',*,*,#3614,.F.);
#5109=ORIENTED_EDGE('',*,*,#3615,.F.);
#5110=ORIENTED_EDGE('',*,*,#3616,.T.);
#5111=ORIENTED_EDGE('',*,*,#3617,.T.);
#5112=ORIENTED_EDGE('',*,*,#3616,.F.);
#5113=ORIENTED_EDGE('',*,*,#3615,.T.);
#5114=ORIENTED_EDGE('',*,*,#3618,.F.);
#5115=ORIENTED_EDGE('',*,*,#3618,.T.);
#5116=ORIENTED_EDGE('',*,*,#3619,.T.);
#5117=ORIENTED_EDGE('',*,*,#3620,.T.);
#5118=ORIENTED_EDGE('',*,*,#3621,.T.);
#5119=ORIENTED_EDGE('',*,*,#3622,.T.);
#5120=ORIENTED_EDGE('',*,*,#3623,.T.);
#5121=ORIENTED_EDGE('',*,*,#3624,.T.);
#5122=ORIENTED_EDGE('',*,*,#3617,.F.);
#5123=ORIENTED_EDGE('',*,*,#3608,.T.);
#5124=ORIENTED_EDGE('',*,*,#3613,.F.);
#5125=ORIENTED_EDGE('',*,*,#3625,.T.);
#5126=ORIENTED_EDGE('',*,*,#3626,.T.);
#5127=ORIENTED_EDGE('',*,*,#3627,.T.);
#5128=ORIENTED_EDGE('',*,*,#3620,.F.);
#5129=ORIENTED_EDGE('',*,*,#3628,.F.);
#5130=ORIENTED_EDGE('',*,*,#3629,.T.);
#5131=ORIENTED_EDGE('',*,*,#3630,.T.);
#5132=ORIENTED_EDGE('',*,*,#3631,.T.);
#5133=ORIENTED_EDGE('',*,*,#3621,.F.);
#5134=ORIENTED_EDGE('',*,*,#3627,.F.);
#5135=ORIENTED_EDGE('',*,*,#3632,.T.);
#5136=ORIENTED_EDGE('',*,*,#3633,.T.);
#5137=ORIENTED_EDGE('',*,*,#3634,.T.);
#5138=ORIENTED_EDGE('',*,*,#3622,.F.);
#5139=ORIENTED_EDGE('',*,*,#3631,.F.);
#5140=ORIENTED_EDGE('',*,*,#3635,.T.);
#5141=ORIENTED_EDGE('',*,*,#3636,.T.);
#5142=ORIENTED_EDGE('',*,*,#3637,.T.);
#5143=ORIENTED_EDGE('',*,*,#3623,.F.);
#5144=ORIENTED_EDGE('',*,*,#3634,.F.);
#5145=ORIENTED_EDGE('',*,*,#3638,.T.);
#5146=ORIENTED_EDGE('',*,*,#3639,.T.);
#5147=ORIENTED_EDGE('',*,*,#3640,.T.);
#5148=ORIENTED_EDGE('',*,*,#3624,.F.);
#5149=ORIENTED_EDGE('',*,*,#3637,.F.);
#5150=ORIENTED_EDGE('',*,*,#3641,.T.);
#5151=ORIENTED_EDGE('',*,*,#3642,.T.);
#5152=ORIENTED_EDGE('',*,*,#3628,.T.);
#5153=ORIENTED_EDGE('',*,*,#3619,.F.);
#5154=ORIENTED_EDGE('',*,*,#3640,.F.);
#5155=ORIENTED_EDGE('',*,*,#3607,.F.);
#5156=ORIENTED_EDGE('',*,*,#3635,.F.);
#5157=ORIENTED_EDGE('',*,*,#3633,.F.);
#5158=ORIENTED_EDGE('',*,*,#3606,.F.);
#5159=ORIENTED_EDGE('',*,*,#3638,.F.);
#5160=ORIENTED_EDGE('',*,*,#3636,.F.);
#5161=ORIENTED_EDGE('',*,*,#3605,.F.);
#5162=ORIENTED_EDGE('',*,*,#3641,.F.);
#5163=ORIENTED_EDGE('',*,*,#3639,.F.);
#5164=ORIENTED_EDGE('',*,*,#3604,.F.);
#5165=ORIENTED_EDGE('',*,*,#3625,.F.);
#5166=ORIENTED_EDGE('',*,*,#3642,.F.);
#5167=ORIENTED_EDGE('',*,*,#3603,.F.);
#5168=ORIENTED_EDGE('',*,*,#3629,.F.);
#5169=ORIENTED_EDGE('',*,*,#3626,.F.);
#5170=ORIENTED_EDGE('',*,*,#3602,.F.);
#5171=ORIENTED_EDGE('',*,*,#3632,.F.);
#5172=ORIENTED_EDGE('',*,*,#3630,.F.);
#5265=CYLINDRICAL_SURFACE('',#6166,1.5);
#5266=CYLINDRICAL_SURFACE('',#6167,2.85);
#5557=ADVANCED_FACE('',(#840),#165,.F.);
#5558=ADVANCED_FACE('',(#841),#158,.F.);
#5559=ADVANCED_FACE('',(#842),#166,.T.);
#5560=ADVANCED_FACE('',(#843),#5265,.T.);
#5561=ADVANCED_FACE('',(#844),#5266,.T.);
#5562=ADVANCED_FACE('',(#845,#386),#154,.T.);
#5563=ADVANCED_FACE('',(#846,#387),#535,.T.);
#5564=ADVANCED_FACE('',(#847,#388),#536,.F.);
#5565=ADVANCED_FACE('',(#848),#537,.F.);
#5566=ADVANCED_FACE('',(#849),#538,.T.);
#5567=ADVANCED_FACE('',(#850),#539,.T.);
#5568=ADVANCED_FACE('',(#851),#540,.T.);
#5569=ADVANCED_FACE('',(#852),#541,.T.);
#5570=ADVANCED_FACE('',(#853),#542,.T.);
#5571=ADVANCED_FACE('',(#854),#543,.T.);
#5572=ADVANCED_FACE('',(#855),#544,.F.);
#5573=ADVANCED_FACE('',(#856),#545,.F.);
#5574=ADVANCED_FACE('',(#857),#546,.F.);
#5575=ADVANCED_FACE('',(#858),#547,.F.);
#5576=ADVANCED_FACE('',(#859),#548,.F.);
#5577=ADVANCED_FACE('',(#860),#549,.F.);
#5589=CLOSED_SHELL('',(#5557,#5558,#5559,#5560,#5561,#5562,#5563,#5564,
#5565,#5566,#5567,#5568,#5569,#5570,#5571,#5572,#5573,#5574,#5575,#5576,
#5577));
#6151=AXIS2_PLACEMENT_3D('',#12822,#7595,#7596);
#6152=AXIS2_PLACEMENT_3D('',#12823,#7597,#7598);
#6153=AXIS2_PLACEMENT_3D('',#12828,#7600,#7601);
#6154=AXIS2_PLACEMENT_3D('',#12830,#7602,#7603);
#6155=AXIS2_PLACEMENT_3D('',#12832,#7604,#7605);
#6156=AXIS2_PLACEMENT_3D('',#12834,#7606,#7607);
#6157=AXIS2_PLACEMENT_3D('',#12836,#7608,#7609);
#6158=AXIS2_PLACEMENT_3D('',#12837,#7610,#7611);
#6159=AXIS2_PLACEMENT_3D('',#12838,#7612,#7613);
#6160=AXIS2_PLACEMENT_3D('',#12840,#7614,#7615);
#6161=AXIS2_PLACEMENT_3D('',#12842,#7616,#7617);
#6162=AXIS2_PLACEMENT_3D('',#12843,#7618,#7619);
#6163=AXIS2_PLACEMENT_3D('',#12844,#7620,#7621);
#6164=AXIS2_PLACEMENT_3D('',#12846,#7622,#7623);
#6165=AXIS2_PLACEMENT_3D('',#12849,#7625,#7626);
#6166=AXIS2_PLACEMENT_3D('',#12850,#7627,#7628);
#6167=AXIS2_PLACEMENT_3D('',#12852,#7630,#7631);
#6168=AXIS2_PLACEMENT_3D('',#12854,#7632,#7633);
#6169=AXIS2_PLACEMENT_3D('',#12857,#7635,#7636);
#6170=AXIS2_PLACEMENT_3D('',#12858,#7637,#7638);
#6171=AXIS2_PLACEMENT_3D('',#12860,#7639,#7640);
#6172=AXIS2_PLACEMENT_3D('',#12861,#7641,#7642);
#6173=AXIS2_PLACEMENT_3D('',#12874,#7649,#7650);
#6174=AXIS2_PLACEMENT_3D('',#12875,#7651,#7652);
#6175=AXIS2_PLACEMENT_3D('',#12876,#7653,#7654);
#6176=AXIS2_PLACEMENT_3D('',#12883,#7659,#7660);
#6177=AXIS2_PLACEMENT_3D('',#12888,#7664,#7665);
#6178=AXIS2_PLACEMENT_3D('',#12893,#7669,#7670);
#6179=AXIS2_PLACEMENT_3D('',#12898,#7674,#7675);
#6180=AXIS2_PLACEMENT_3D('',#12903,#7679,#7680);
#6181=AXIS2_PLACEMENT_3D('',#12906,#7683,#7684);
#6182=AXIS2_PLACEMENT_3D('',#12907,#7685,#7686);
#6183=AXIS2_PLACEMENT_3D('',#12908,#7687,#7688);
#6184=AXIS2_PLACEMENT_3D('',#12909,#7689,#7690);
#6185=AXIS2_PLACEMENT_3D('',#12910,#7691,#7692);
#6186=AXIS2_PLACEMENT_3D('',#12911,#7693,#7694);
#7595=DIRECTION('axis',(0.,0.,1.));
#7596=DIRECTION('refdir',(1.,0.,0.));
#7597=DIRECTION('center_axis',(-1.,0.,0.));
#7598=DIRECTION('ref_axis',(0.,0.,1.));
#7599=DIRECTION('',(-0.500000000000004,-1.0605752387249E-16,-0.866025403784436));
#7600=DIRECTION('center_axis',(-1.,0.,0.));
#7601=DIRECTION('ref_axis',(0.,0.,1.));
#7602=DIRECTION('center_axis',(-1.,0.,0.));
#7603=DIRECTION('ref_axis',(0.,0.,1.));
#7604=DIRECTION('center_axis',(-1.,0.,0.));
#7605=DIRECTION('ref_axis',(0.,0.,1.));
#7606=DIRECTION('center_axis',(-1.,0.,0.));
#7607=DIRECTION('ref_axis',(0.,0.,1.));
#7608=DIRECTION('center_axis',(-1.,0.,0.));
#7609=DIRECTION('ref_axis',(0.,0.,1.));
#7610=DIRECTION('center_axis',(-1.,0.,0.));
#7611=DIRECTION('ref_axis',(0.,0.,1.));
#7612=DIRECTION('center_axis',(-1.,0.,0.));
#7613=DIRECTION('ref_axis',(0.,0.,1.));
#7614=DIRECTION('center_axis',(-1.,0.,0.));
#7615=DIRECTION('ref_axis',(0.,0.,1.));
#7616=DIRECTION('center_axis',(0.,1.,-1.22464679914735E-16));
#7617=DIRECTION('ref_axis',(0.,-1.22464679914735E-16,-1.));
#7618=DIRECTION('center_axis',(1.,0.,0.));
#7619=DIRECTION('ref_axis',(0.,0.,1.));
#7620=DIRECTION('center_axis',(-1.,0.,0.));
#7621=DIRECTION('ref_axis',(0.,0.,1.));
#7622=DIRECTION('center_axis',(-1.,0.,0.));
#7623=DIRECTION('ref_axis',(0.,0.,1.));
#7624=DIRECTION('',(0.707106781186549,8.65956056235491E-17,0.707106781186546));
#7625=DIRECTION('center_axis',(-1.,0.,0.));
#7626=DIRECTION('ref_axis',(0.,0.,1.));
#7627=DIRECTION('center_axis',(-1.,0.,0.));
#7628=DIRECTION('ref_axis',(0.,0.,1.));
#7629=DIRECTION('',(1.,0.,0.));
#7630=DIRECTION('center_axis',(-1.,0.,0.));
#7631=DIRECTION('ref_axis',(0.,0.,1.));
#7632=DIRECTION('center_axis',(-1.,0.,0.));
#7633=DIRECTION('ref_axis',(0.,0.,1.));
#7634=DIRECTION('',(1.,0.,0.));
#7635=DIRECTION('center_axis',(-1.,0.,0.));
#7636=DIRECTION('ref_axis',(0.,0.,1.));
#7637=DIRECTION('center_axis',(0.,6.12323399573677E-17,-1.));
#7638=DIRECTION('ref_axis',(0.,1.,0.));
#7639=DIRECTION('center_axis',(-1.,0.,0.));
#7640=DIRECTION('ref_axis',(0.,0.,1.));
#7641=DIRECTION('center_axis',(-1.,0.,0.));
#7642=DIRECTION('ref_axis',(0.,0.,1.));
#7643=DIRECTION('',(0.,-1.,-1.87789324842145E-16));
#7644=DIRECTION('',(0.,-0.5,-0.866025403784438));
#7645=DIRECTION('',(0.,0.5,-0.866025403784438));
#7646=DIRECTION('',(0.,1.,0.));
#7647=DIRECTION('',(0.,0.5,0.866025403784438));
#7648=DIRECTION('',(0.,-0.5,0.866025403784438));
#7649=DIRECTION('center_axis',(-1.,0.,0.));
#7650=DIRECTION('ref_axis',(0.,0.,1.));
#7651=DIRECTION('center_axis',(-1.,0.,0.));
#7652=DIRECTION('ref_axis',(0.,0.,1.));
#7653=DIRECTION('center_axis',(0.,0.866025403784438,-0.5));
#7654=DIRECTION('ref_axis',(0.,0.5,0.866025403784438));
#7655=DIRECTION('',(0.,-0.5,-0.866025403784438));
#7656=DIRECTION('',(0.,-0.5,-0.866025403784438));
#7657=DIRECTION('',(-1.,0.,0.));
#7658=DIRECTION('',(-1.,0.,0.));
#7659=DIRECTION('center_axis',(0.,0.866025403784438,0.5));
#7660=DIRECTION('ref_axis',(0.,-0.5,0.866025403784438));
#7661=DIRECTION('',(0.,0.5,-0.866025403784438));
#7662=DIRECTION('',(0.,0.5,-0.866025403784438));
#7663=DIRECTION('',(-1.,0.,0.));
#7664=DIRECTION('center_axis',(0.,0.,1.));
#7665=DIRECTION('ref_axis',(1.,0.,0.));
#7666=DIRECTION('',(0.,1.,0.));
#7667=DIRECTION('',(0.,1.,0.));
#7668=DIRECTION('',(-1.,0.,0.));
#7669=DIRECTION('center_axis',(0.,-0.866025403784438,0.5));
#7670=DIRECTION('ref_axis',(0.,-0.5,-0.866025403784438));
#7671=DIRECTION('',(0.,0.5,0.866025403784438));
#7672=DIRECTION('',(0.,0.5,0.866025403784438));
#7673=DIRECTION('',(-1.,0.,0.));
#7674=DIRECTION('center_axis',(0.,-0.866025403784439,-0.5));
#7675=DIRECTION('ref_axis',(0.,0.5,-0.866025403784439));
#7676=DIRECTION('',(0.,-0.5,0.866025403784438));
#7677=DIRECTION('',(0.,-0.5,0.866025403784438));
#7678=DIRECTION('',(-1.,0.,0.));
#7679=DIRECTION('center_axis',(0.,1.87789324842145E-16,-1.));
#7680=DIRECTION('ref_axis',(0.,1.,1.87789324842145E-16));
#7681=DIRECTION('',(0.,-1.,-1.87789324842145E-16));
#7682=DIRECTION('',(0.,-1.,-1.87789324842145E-16));
#7683=DIRECTION('center_axis',(1.,0.,0.));
#7684=DIRECTION('ref_axis',(0.,0.,-1.));
#7685=DIRECTION('center_axis',(1.,0.,0.));
#7686=DIRECTION('ref_axis',(0.,0.,-1.));
#7687=DIRECTION('center_axis',(1.,0.,0.));
#7688=DIRECTION('ref_axis',(0.,0.,-1.));
#7689=DIRECTION('center_axis',(1.,0.,0.));
#7690=DIRECTION('ref_axis',(0.,0.,-1.));
#7691=DIRECTION('center_axis',(1.,0.,0.));
#7692=DIRECTION('ref_axis',(0.,0.,-1.));
#7693=DIRECTION('center_axis',(1.,0.,0.));
#7694=DIRECTION('ref_axis',(0.,0.,-1.));
#12822=CARTESIAN_POINT('',(0.,0.,0.));
#12823=CARTESIAN_POINT('Origin',(-998.38264973081,0.,0.));
#12824=CARTESIAN_POINT('',(1.61735026918963,2.10855288962746E-17,0.));
#12825=CARTESIAN_POINT('',(1.04,0.,-1.));
#12826=CARTESIAN_POINT('',(-998.38264973081,-2.12115047744979E-13,-1732.05080756886));
#12827=CARTESIAN_POINT('',(1.04,-0.866025403784438,-0.5));
#12828=CARTESIAN_POINT('Origin',(1.04,0.,0.));
#12829=CARTESIAN_POINT('',(1.04,-0.866025403784439,0.5));
#12830=CARTESIAN_POINT('Origin',(1.04,0.,0.));
#12831=CARTESIAN_POINT('',(1.04,-1.87789324842145E-16,1.));
#12832=CARTESIAN_POINT('Origin',(1.04,0.,0.));
#12833=CARTESIAN_POINT('',(1.04,0.866025403784439,0.500000000000001));
#12834=CARTESIAN_POINT('Origin',(1.04,0.,0.));
#12835=CARTESIAN_POINT('',(1.04,0.866025403784439,-0.500000000000001));
#12836=CARTESIAN_POINT('Origin',(1.04,0.,0.));
#12837=CARTESIAN_POINT('Origin',(1.04,0.,0.));
#12838=CARTESIAN_POINT('Origin',(1.75,0.,0.));
#12839=CARTESIAN_POINT('',(1.65,-1.95943487863576E-16,-1.6));
#12840=CARTESIAN_POINT('Origin',(1.65,0.,0.));
#12841=CARTESIAN_POINT('',(1.75,-1.83697019872103E-16,-1.5));
#12842=CARTESIAN_POINT('Origin',(1.75,-1.95943487863576E-16,-1.6));
#12843=CARTESIAN_POINT('Origin',(1.75,0.,0.));
#12844=CARTESIAN_POINT('Origin',(4.65,0.,0.));
#12845=CARTESIAN_POINT('',(4.3695,-1.83697019872103E-16,-1.5));
#12846=CARTESIAN_POINT('Origin',(4.3695,0.,0.));
#12847=CARTESIAN_POINT('',(4.65,-1.4934567715602E-16,-1.2195));
#12848=CARTESIAN_POINT('',(4.65,-1.4934567715602E-16,-1.2195));
#12849=CARTESIAN_POINT('Origin',(4.65,0.,0.));
#12850=CARTESIAN_POINT('Origin',(0.,0.,0.));
#12851=CARTESIAN_POINT('',(0.,-1.83697019872103E-16,-1.5));
#12852=CARTESIAN_POINT('Origin',(0.,0.,0.));
#12853=CARTESIAN_POINT('',(1.27,-3.49024337756996E-16,-2.85));
#12854=CARTESIAN_POINT('Origin',(1.27,0.,0.));
#12855=CARTESIAN_POINT('',(1.65,-3.49024337756996E-16,-2.85));
#12856=CARTESIAN_POINT('',(0.,-3.49024337756996E-16,-2.85));
#12857=CARTESIAN_POINT('Origin',(1.65,0.,0.));
#12858=CARTESIAN_POINT('Origin',(3.03337598425197,-4.33680868994202E-16,
0.));
#12859=CARTESIAN_POINT('',(4.33680868994202E-16,1.425,0.));
#12860=CARTESIAN_POINT('Origin',(4.33680868994202E-16,0.,0.));
#12861=CARTESIAN_POINT('Origin',(2.16840434497101E-16,0.,0.));
#12862=CARTESIAN_POINT('',(0.,0.577350269189626,1.));
#12863=CARTESIAN_POINT('',(2.16840434497101E-16,-0.577350269189626,1.));
#12864=CARTESIAN_POINT('',(0.,-0.577350269189626,1.));
#12865=CARTESIAN_POINT('',(0.,-1.15470053837925,-9.88971598953938E-18));
#12866=CARTESIAN_POINT('',(0.,-1.15470053837925,-9.88971598953938E-18));
#12867=CARTESIAN_POINT('',(0.,-0.577350269189625,-1.));
#12868=CARTESIAN_POINT('',(0.,-0.577350269189625,-1.));
#12869=CARTESIAN_POINT('',(0.,0.577350269189626,-1.));
#12870=CARTESIAN_POINT('',(0.,0.577350269189626,-1.));
#12871=CARTESIAN_POINT('',(0.,1.15470053837925,-1.08420217247849E-16));
#12872=CARTESIAN_POINT('',(0.,1.15470053837925,-1.08420217247849E-16));
#12873=CARTESIAN_POINT('',(0.,0.577350269189626,1.));
#12874=CARTESIAN_POINT('Origin',(1.65,1.5,0.));
#12875=CARTESIAN_POINT('Origin',(4.65,0.,0.));
#12876=CARTESIAN_POINT('Origin',(1.04,-1.15470053837925,-9.88971598953938E-18));
#12877=CARTESIAN_POINT('',(1.04,-0.577350269189626,1.));
#12878=CARTESIAN_POINT('',(1.04,-1.15470053837925,-9.88971598953938E-18));
#12879=CARTESIAN_POINT('',(1.04,-1.15470053837925,-9.88971598953938E-18));
#12880=CARTESIAN_POINT('',(1.04,-1.15470053837925,-9.88971598953938E-18));
#12881=CARTESIAN_POINT('',(1.04,-1.15470053837925,-9.88971598953938E-18));
#12882=CARTESIAN_POINT('',(1.04,-0.577350269189626,1.));
#12883=CARTESIAN_POINT('Origin',(1.04,-0.577350269189625,-1.));
#12884=CARTESIAN_POINT('',(1.04,-0.577350269189625,-1.));
#12885=CARTESIAN_POINT('',(1.04,-0.577350269189625,-1.));
#12886=CARTESIAN_POINT('',(1.04,-0.577350269189625,-1.));
#12887=CARTESIAN_POINT('',(1.04,-0.577350269189625,-1.));
#12888=CARTESIAN_POINT('Origin',(1.04,0.577350269189626,-1.));
#12889=CARTESIAN_POINT('',(1.04,0.577350269189626,-1.));
#12890=CARTESIAN_POINT('',(1.04,0.577350269189626,-1.));
#12891=CARTESIAN_POINT('',(1.04,0.577350269189626,-1.));
#12892=CARTESIAN_POINT('',(1.04,0.577350269189626,-1.));
#12893=CARTESIAN_POINT('Origin',(1.04,1.15470053837925,-1.08420217247849E-16));
#12894=CARTESIAN_POINT('',(1.04,1.15470053837925,-1.08420217247849E-16));
#12895=CARTESIAN_POINT('',(1.04,1.15470053837925,-1.08420217247849E-16));
#12896=CARTESIAN_POINT('',(1.04,1.15470053837925,-1.08420217247849E-16));
#12897=CARTESIAN_POINT('',(1.04,1.15470053837925,-1.08420217247849E-16));
#12898=CARTESIAN_POINT('Origin',(1.04,0.577350269189626,1.));
#12899=CARTESIAN_POINT('',(1.04,0.577350269189626,1.));
#12900=CARTESIAN_POINT('',(1.04,0.577350269189626,1.));
#12901=CARTESIAN_POINT('',(1.04,0.577350269189626,1.));
#12902=CARTESIAN_POINT('',(1.04,0.577350269189626,1.));
#12903=CARTESIAN_POINT('Origin',(1.04,-0.577350269189626,1.));
#12904=CARTESIAN_POINT('',(1.04,-0.577350269189626,1.));
#12905=CARTESIAN_POINT('',(1.04,-0.577350269189626,1.));
#12906=CARTESIAN_POINT('Origin',(1.04,-1.15470053837925,0.));
#12907=CARTESIAN_POINT('Origin',(1.04,-1.15470053837925,0.));
#12908=CARTESIAN_POINT('Origin',(1.04,-1.15470053837925,0.));
#12909=CARTESIAN_POINT('Origin',(1.04,-1.15470053837925,0.));
#12910=CARTESIAN_POINT('Origin',(1.04,-1.15470053837925,0.));
#12911=CARTESIAN_POINT('Origin',(1.04,-1.15470053837925,0.));
#12955=UNCERTAINTY_MEASURE_WITH_UNIT(LENGTH_MEASURE(0.01),#12967,
'DISTANCE_ACCURACY_VALUE',
'Maximum model space distance between geometric entities at asserted c
onnectivities');
#12956=UNCERTAINTY_MEASURE_WITH_UNIT(LENGTH_MEASURE(0.01),#12967,
'DISTANCE_ACCURACY_VALUE',
'Maximum model space distance between geometric entities at asserted c
onnectivities');
#12965=(
GEOMETRIC_REPRESENTATION_CONTEXT(3)
GLOBAL_UNCERTAINTY_ASSIGNED_CONTEXT((#12955))
GLOBAL_UNIT_ASSIGNED_CONTEXT((#12967,#12969,#12970))
REPRESENTATION_CONTEXT('','3D')
);
#12966=(
GEOMETRIC_REPRESENTATION_CONTEXT(3)
GLOBAL_UNCERTAINTY_ASSIGNED_CONTEXT((#12956))
GLOBAL_UNIT_ASSIGNED_CONTEXT((#12967,#12969,#12970))
REPRESENTATION_CONTEXT('','3D')
);
#12967=(
LENGTH_UNIT()
NAMED_UNIT(*)
SI_UNIT(.MILLI.,.METRE.)
);
#12969=(
NAMED_UNIT(*)
PLANE_ANGLE_UNIT()
SI_UNIT($,.RADIAN.)
);
#12970=(
NAMED_UNIT(*)
SI_UNIT($,.STERADIAN.)
SOLID_ANGLE_UNIT()
);
#12979=SHAPE_DEFINITION_REPRESENTATION(#12988,#13032);
#12988=PRODUCT_DEFINITION_SHAPE('',$,#13042);
#13032=SHAPE_REPRESENTATION('',(#6151),#12965);
#13033=PRODUCT_DEFINITION_CONTEXT('part definition',#13062,'design');
#13042=PRODUCT_DEFINITION('Button Head Cap Screw M3x0.5x3',
'Button Head Cap Screw M3x0.5x3',#13051,#13033);
#13051=PRODUCT_DEFINITION_FORMATION('',$,#13072);
#13062=APPLICATION_CONTEXT(
'Core Data for Automotive Mechanical Design Process');
#13063=PRODUCT_CONTEXT('part definition',#13062,'mechanical');
#13072=PRODUCT('Button Head Cap Screw M3x0.5x3',
'Button Head Cap Screw M3x0.5x3',$,(#13063));
#13075=PRESENTATION_STYLE_ASSIGNMENT((#13080));
#13080=SURFACE_STYLE_USAGE(.BOTH.,#13085);
#13085=SURFACE_SIDE_STYLE('',(#13090));
#13090=SURFACE_STYLE_FILL_AREA(#13095);
#13095=FILL_AREA_STYLE('Opaque(31,36,43)',(#13100));
#13100=FILL_AREA_STYLE_COLOUR('Opaque(31,36,43)',#13105);
#13105=COLOUR_RGB('Opaque(31,36,43)',0.12156862745098,0.141176470588235,
0.168627450980392);
ENDSEC;
END-ISO-10303-21;
